ISO-10303-21;
HEADER;
FILE_DESCRIPTION((''),'2;1');
FILE_NAME('Cover_Screw_2.step','2026-10-09T10:11:57-07:00',(''),(''),'','','');
FILE_SCHEMA (('AUTOMOTIVE_DESIGN { 1 0 10303 214 3 1 1 }'));
ENDSEC;
DATA;
#10=MECHANICAL_DESIGN_GEOMETRIC_PRESENTATION_REPRESENTATION('',(#130),#13510);
#100=SHAPE_REPRESENTATION_RELATIONSHIP('SRR','None',#13570,#115) ;
#115=ADVANCED_BREP_SHAPE_REPRESENTATION('',(#162),#13502) ;
#130=STYLED_ITEM('',(#13650),#162) ;
#162=MANIFOLD_SOLID_BREP('Body1',#7379) ;
#244=FACE_BOUND('',#1468,.T.) ;
#416=PLANE('',#8204) ;
#417=PLANE('',#8205) ;
#418=PLANE('',#8206) ;
#419=PLANE('',#8207) ;
#420=PLANE('',#8208) ;
#421=PLANE('',#8209) ;
#422=PLANE('',#8210) ;
#423=PLANE('',#8211) ;
#424=PLANE('',#8212) ;
#425=PLANE('',#8213) ;
#426=PLANE('',#8214) ;
#427=PLANE('',#8215) ;
#428=PLANE('',#8216) ;
#429=PLANE('',#8217) ;
#430=PLANE('',#8218) ;
#431=PLANE('',#8219) ;
#432=PLANE('',#8220) ;
#433=PLANE('',#8221) ;
#434=PLANE('',#8222) ;
#640=CYLINDRICAL_SURFACE('',#8195,2.6) ;
#641=CYLINDRICAL_SURFACE('',#8200,1.5) ;
#949=FACE_OUTER_BOUND('',#1454,.T.) ;
#950=FACE_OUTER_BOUND('',#1455,.T.) ;
#951=FACE_OUTER_BOUND('',#1456,.T.) ;
#952=FACE_OUTER_BOUND('',#1457,.T.) ;
#953=FACE_OUTER_BOUND('',#1458,.T.) ;
#954=FACE_OUTER_BOUND('',#1459,.T.) ;
#955=FACE_OUTER_BOUND('',#1460,.T.) ;
#956=FACE_OUTER_BOUND('',#1461,.T.) ;
#957=FACE_OUTER_BOUND('',#1462,.T.) ;
#958=FACE_OUTER_BOUND('',#1463,.T.) ;
#959=FACE_OUTER_BOUND('',#1464,.T.) ;
#960=FACE_OUTER_BOUND('',#1465,.T.) ;
#961=FACE_OUTER_BOUND('',#1466,.T.) ;
#962=FACE_OUTER_BOUND('',#1467,.T.) ;
#963=FACE_OUTER_BOUND('',#1469,.T.) ;
#964=FACE_OUTER_BOUND('',#1470,.T.) ;
#965=FACE_OUTER_BOUND('',#1471,.T.) ;
#966=FACE_OUTER_BOUND('',#1472,.T.) ;
#967=FACE_OUTER_BOUND('',#1473,.T.) ;
#968=FACE_OUTER_BOUND('',#1474,.T.) ;
#969=FACE_OUTER_BOUND('',#1475,.T.) ;
#970=FACE_OUTER_BOUND('',#1476,.T.) ;
#971=FACE_OUTER_BOUND('',#1477,.T.) ;
#1454=EDGE_LOOP('',(#6244,#6245,#6246,#6247)) ;
#1455=EDGE_LOOP('',(#6248,#6249,#6250,#6251)) ;
#1456=EDGE_LOOP('',(#6252,#6253,#6254,#6255)) ;
#1457=EDGE_LOOP('',(#6256,#6257,#6258,#6259)) ;
#1458=EDGE_LOOP('',(#6260)) ;
#1459=EDGE_LOOP('',(#6261,#6262,#6263,#6264)) ;
#1460=EDGE_LOOP('',(#6265,#6266,#6267,#6268)) ;
#1461=EDGE_LOOP('',(#6269,#6270,#6271,#6272)) ;
#1462=EDGE_LOOP('',(#6273,#6274,#6275,#6276)) ;
#1463=EDGE_LOOP('',(#6277,#6278,#6279,#6280)) ;
#1464=EDGE_LOOP('',(#6281,#6282,#6283,#6284)) ;
#1465=EDGE_LOOP('',(#6285,#6286,#6287,#6288)) ;
#1466=EDGE_LOOP('',(#6289,#6290,#6291,#6292)) ;
#1467=EDGE_LOOP('',(#6293)) ;
#1468=EDGE_LOOP('',(#6294,#6295,#6296,#6297,#6298,#6299,#6300,#6301,#6302,
#6303,#6304,#6305)) ;
#1469=EDGE_LOOP('',(#6306,#6307,#6308,#6309)) ;
#1470=EDGE_LOOP('',(#6310,#6311,#6312,#6313)) ;
#1471=EDGE_LOOP('',(#6314,#6315,#6316,#6317)) ;
#1472=EDGE_LOOP('',(#6318,#6319,#6320,#6321)) ;
#1473=EDGE_LOOP('',(#6322,#6323,#6324,#6325)) ;
#1474=EDGE_LOOP('',(#6326,#6327,#6328,#6329)) ;
#1475=EDGE_LOOP('',(#6330,#6331,#6332,#6333)) ;
#1476=EDGE_LOOP('',(#6334,#6335,#6336,#6337)) ;
#1477=EDGE_LOOP('',(#6338,#6339,#6340,#6341)) ;
#2007=LINE('',#12769,#2501) ;
#2008=LINE('',#12773,#2502) ;
#2009=LINE('',#12777,#2503) ;
#2010=LINE('',#12781,#2504) ;
#2011=LINE('',#12787,#2505) ;
#2012=LINE('',#12789,#2506) ;
#2013=LINE('',#12791,#2507) ;
#2014=LINE('',#12792,#2508) ;
#2015=LINE('',#12796,#2509) ;
#2016=LINE('',#12798,#2510) ;
#2017=LINE('',#12800,#2511) ;
#2018=LINE('',#12801,#2512) ;
#2019=LINE('',#12804,#2513) ;
#2020=LINE('',#12806,#2514) ;
#2021=LINE('',#12807,#2515) ;
#2022=LINE('',#12811,#2516) ;
#2023=LINE('',#12812,#2517) ;
#2024=LINE('',#12813,#2518) ;
#2025=LINE('',#12816,#2519) ;
#2026=LINE('',#12817,#2520) ;
#2027=LINE('',#12820,#2521) ;
#2028=LINE('',#12821,#2522) ;
#2029=LINE('',#12824,#2523) ;
#2030=LINE('',#12825,#2524) ;
#2031=LINE('',#12828,#2525) ;
#2032=LINE('',#12829,#2526) ;
#2033=LINE('',#12832,#2527) ;
#2034=LINE('',#12834,#2528) ;
#2035=LINE('',#12835,#2529) ;
#2036=LINE('',#12837,#2530) ;
#2037=LINE('',#12839,#2531) ;
#2038=LINE('',#12840,#2532) ;
#2039=LINE('',#12844,#2533) ;
#2040=LINE('',#12845,#2534) ;
#2041=LINE('',#12846,#2535) ;
#2042=LINE('',#12847,#2536) ;
#2043=LINE('',#12849,#2537) ;
#2044=LINE('',#12850,#2538) ;
#2045=LINE('',#12854,#2539) ;
#2046=LINE('',#12856,#2540) ;
#2047=LINE('',#12858,#2541) ;
#2048=LINE('',#12859,#2542) ;
#2049=LINE('',#12861,#2543) ;
#2050=LINE('',#12863,#2544) ;
#2501=VECTOR('',#10179,2.6) ;
#2502=VECTOR('',#10184,1.5) ;
#2503=VECTOR('',#10189,1.5) ;
#2504=VECTOR('',#10194,1.2) ;
#2505=VECTOR('',#10201,0.99999999999962) ;
#2506=VECTOR('',#10202,1.00000000000035) ;
#2507=VECTOR('',#10203,0.99999999999962) ;
#2508=VECTOR('',#10204,1.00000000000035) ;
#2509=VECTOR('',#10207,0.99999999999962) ;
#2510=VECTOR('',#10208,1.00000000000035) ;
#2511=VECTOR('',#10209,0.99999999999962) ;
#2512=VECTOR('',#10210,1.00000000000035) ;
#2513=VECTOR('',#10213,1.) ;
#2514=VECTOR('',#10214,0.99999999999962) ;
#2515=VECTOR('',#10215,1.) ;
#2516=VECTOR('',#10218,0.99999999999962) ;
#2517=VECTOR('',#10219,1.) ;
#2518=VECTOR('',#10220,1.) ;
#2519=VECTOR('',#10223,0.99999999999962) ;
#2520=VECTOR('',#10224,1.) ;
#2521=VECTOR('',#10227,0.99999999999962) ;
#2522=VECTOR('',#10228,1.) ;
#2523=VECTOR('',#10231,1.) ;
#2524=VECTOR('',#10232,0.99999999999962) ;
#2525=VECTOR('',#10235,1.) ;
#2526=VECTOR('',#10236,0.99999999999962) ;
#2527=VECTOR('',#10239,0.99999999999962) ;
#2528=VECTOR('',#10240,0.99999999999962) ;
#2529=VECTOR('',#10241,0.99999999999962) ;
#2530=VECTOR('',#10242,0.99999999999962) ;
#2531=VECTOR('',#10243,0.99999999999962) ;
#2532=VECTOR('',#10244,0.99999999999962) ;
#2533=VECTOR('',#10247,0.99999999999962) ;
#2534=VECTOR('',#10248,1.00000000000035) ;
#2535=VECTOR('',#10249,0.99999999999962) ;
#2536=VECTOR('',#10250,1.00000000000035) ;
#2537=VECTOR('',#10253,1.) ;
#2538=VECTOR('',#10254,1.) ;
#2539=VECTOR('',#10261,0.99999999999962) ;
#2540=VECTOR('',#10262,1.00000000000035) ;
#2541=VECTOR('',#10263,0.99999999999962) ;
#2542=VECTOR('',#10264,1.00000000000035) ;
#2543=VECTOR('',#10267,1.) ;
#2544=VECTOR('',#10270,1.) ;
#2966=CIRCLE('',#8196,2.6) ;
#2967=CIRCLE('',#8197,2.6) ;
#2968=CIRCLE('',#8199,1.5) ;
#2969=CIRCLE('',#8201,1.5) ;
#2970=CIRCLE('',#8203,1.2) ;
#3594=VERTEX_POINT('',#12766) ;
#3595=VERTEX_POINT('',#12768) ;
#3596=VERTEX_POINT('',#12772) ;
#3597=VERTEX_POINT('',#12776) ;
#3598=VERTEX_POINT('',#12780) ;
#3599=VERTEX_POINT('',#12785) ;
#3600=VERTEX_POINT('',#12786) ;
#3601=VERTEX_POINT('',#12788) ;
#3602=VERTEX_POINT('',#12790) ;
#3603=VERTEX_POINT('',#12794) ;
#3604=VERTEX_POINT('',#12795) ;
#3605=VERTEX_POINT('',#12797) ;
#3606=VERTEX_POINT('',#12799) ;
#3607=VERTEX_POINT('',#12803) ;
#3608=VERTEX_POINT('',#12805) ;
#3609=VERTEX_POINT('',#12809) ;
#3610=VERTEX_POINT('',#12810) ;
#3611=VERTEX_POINT('',#12815) ;
#3612=VERTEX_POINT('',#12819) ;
#3613=VERTEX_POINT('',#12823) ;
#3614=VERTEX_POINT('',#12827) ;
#3615=VERTEX_POINT('',#12831) ;
#3616=VERTEX_POINT('',#12833) ;
#3617=VERTEX_POINT('',#12836) ;
#3618=VERTEX_POINT('',#12838) ;
#3619=VERTEX_POINT('',#12842) ;
#3620=VERTEX_POINT('',#12843) ;
#3621=VERTEX_POINT('',#12855) ;
#3622=VERTEX_POINT('',#12857) ;
#4509=EDGE_CURVE('',#3594,#3594,#2966,.T.) ;
#4510=EDGE_CURVE('',#3594,#3595,#2007,.T.) ;
#4511=EDGE_CURVE('',#3595,#3595,#2967,.T.) ;
#4512=EDGE_CURVE('',#3595,#3596,#2008,.T.) ;
#4513=EDGE_CURVE('',#3596,#3596,#2968,.T.) ;
#4514=EDGE_CURVE('',#3596,#3597,#2009,.T.) ;
#4515=EDGE_CURVE('',#3597,#3597,#2969,.T.) ;
#4516=EDGE_CURVE('',#3597,#3598,#2010,.T.) ;
#4517=EDGE_CURVE('',#3598,#3598,#2970,.T.) ;
#4518=EDGE_CURVE('',#3599,#3600,#2011,.T.) ;
#4519=EDGE_CURVE('',#3599,#3601,#2012,.T.) ;
#4520=EDGE_CURVE('',#3601,#3602,#2013,.T.) ;
#4521=EDGE_CURVE('',#3600,#3602,#2014,.T.) ;
#4522=EDGE_CURVE('',#3603,#3604,#2015,.T.) ;
#4523=EDGE_CURVE('',#3603,#3605,#2016,.F.) ;
#4524=EDGE_CURVE('',#3605,#3606,#2017,.T.) ;
#4525=EDGE_CURVE('',#3604,#3606,#2018,.F.) ;
#4526=EDGE_CURVE('',#3601,#3607,#2019,.T.) ;
#4527=EDGE_CURVE('',#3607,#3608,#2020,.T.) ;
#4528=EDGE_CURVE('',#3602,#3608,#2021,.T.) ;
#4529=EDGE_CURVE('',#3609,#3610,#2022,.T.) ;
#4530=EDGE_CURVE('',#3609,#3603,#2023,.F.) ;
#4531=EDGE_CURVE('',#3610,#3604,#2024,.F.) ;
#4532=EDGE_CURVE('',#3608,#3611,#2025,.T.) ;
#4533=EDGE_CURVE('',#3611,#3600,#2026,.T.) ;
#4534=EDGE_CURVE('',#3612,#3610,#2027,.F.) ;
#4535=EDGE_CURVE('',#3612,#3606,#2028,.T.) ;
#4536=EDGE_CURVE('',#3613,#3599,#2029,.T.) ;
#4537=EDGE_CURVE('',#3607,#3613,#2030,.T.) ;
#4538=EDGE_CURVE('',#3614,#3605,#2031,.T.) ;
#4539=EDGE_CURVE('',#3614,#3609,#2032,.F.) ;
#4540=EDGE_CURVE('',#3613,#3615,#2033,.F.) ;
#4541=EDGE_CURVE('',#3615,#3616,#2034,.T.) ;
#4542=EDGE_CURVE('',#3614,#3616,#2035,.F.) ;
#4543=EDGE_CURVE('',#3617,#3612,#2036,.T.) ;
#4544=EDGE_CURVE('',#3618,#3617,#2037,.T.) ;
#4545=EDGE_CURVE('',#3618,#3611,#2038,.T.) ;
#4546=EDGE_CURVE('',#3619,#3620,#2039,.T.) ;
#4547=EDGE_CURVE('',#3619,#3599,#2040,.F.) ;
#4548=EDGE_CURVE('',#3599,#3605,#2041,.T.) ;
#4549=EDGE_CURVE('',#3620,#3605,#2042,.F.) ;
#4550=EDGE_CURVE('',#3615,#3619,#2043,.F.) ;
#4551=EDGE_CURVE('',#3616,#3620,#2044,.F.) ;
#4552=EDGE_CURVE('',#3600,#3606,#2045,.T.) ;
#4553=EDGE_CURVE('',#3600,#3621,#2046,.T.) ;
#4554=EDGE_CURVE('',#3621,#3622,#2047,.T.) ;
#4555=EDGE_CURVE('',#3606,#3622,#2048,.T.) ;
#4556=EDGE_CURVE('',#3621,#3618,#2049,.T.) ;
#4557=EDGE_CURVE('',#3622,#3617,#2050,.T.) ;
#6244=ORIENTED_EDGE('',*,*,#4509,.F.) ;
#6245=ORIENTED_EDGE('',*,*,#4510,.T.) ;
#6246=ORIENTED_EDGE('',*,*,#4511,.T.) ;
#6247=ORIENTED_EDGE('',*,*,#4510,.F.) ;
#6248=ORIENTED_EDGE('',*,*,#4511,.F.) ;
#6249=ORIENTED_EDGE('',*,*,#4512,.T.) ;
#6250=ORIENTED_EDGE('',*,*,#4513,.T.) ;
#6251=ORIENTED_EDGE('',*,*,#4512,.F.) ;
#6252=ORIENTED_EDGE('',*,*,#4513,.F.) ;
#6253=ORIENTED_EDGE('',*,*,#4514,.T.) ;
#6254=ORIENTED_EDGE('',*,*,#4515,.T.) ;
#6255=ORIENTED_EDGE('',*,*,#4514,.F.) ;
#6256=ORIENTED_EDGE('',*,*,#4515,.F.) ;
#6257=ORIENTED_EDGE('',*,*,#4516,.T.) ;
#6258=ORIENTED_EDGE('',*,*,#4517,.T.) ;
#6259=ORIENTED_EDGE('',*,*,#4516,.F.) ;
#6260=ORIENTED_EDGE('',*,*,#4517,.F.) ;
#6261=ORIENTED_EDGE('',*,*,#4518,.F.) ;
#6262=ORIENTED_EDGE('',*,*,#4519,.T.) ;
#6263=ORIENTED_EDGE('',*,*,#4520,.T.) ;
#6264=ORIENTED_EDGE('',*,*,#4521,.F.) ;
#6265=ORIENTED_EDGE('',*,*,#4522,.F.) ;
#6266=ORIENTED_EDGE('',*,*,#4523,.T.) ;
#6267=ORIENTED_EDGE('',*,*,#4524,.T.) ;
#6268=ORIENTED_EDGE('',*,*,#4525,.F.) ;
#6269=ORIENTED_EDGE('',*,*,#4520,.F.) ;
#6270=ORIENTED_EDGE('',*,*,#4526,.T.) ;
#6271=ORIENTED_EDGE('',*,*,#4527,.T.) ;
#6272=ORIENTED_EDGE('',*,*,#4528,.F.) ;
#6273=ORIENTED_EDGE('',*,*,#4529,.F.) ;
#6274=ORIENTED_EDGE('',*,*,#4530,.T.) ;
#6275=ORIENTED_EDGE('',*,*,#4522,.T.) ;
#6276=ORIENTED_EDGE('',*,*,#4531,.F.) ;
#6277=ORIENTED_EDGE('',*,*,#4521,.T.) ;
#6278=ORIENTED_EDGE('',*,*,#4528,.T.) ;
#6279=ORIENTED_EDGE('',*,*,#4532,.T.) ;
#6280=ORIENTED_EDGE('',*,*,#4533,.T.) ;
#6281=ORIENTED_EDGE('',*,*,#4534,.T.) ;
#6282=ORIENTED_EDGE('',*,*,#4531,.T.) ;
#6283=ORIENTED_EDGE('',*,*,#4525,.T.) ;
#6284=ORIENTED_EDGE('',*,*,#4535,.F.) ;
#6285=ORIENTED_EDGE('',*,*,#4536,.F.) ;
#6286=ORIENTED_EDGE('',*,*,#4537,.F.) ;
#6287=ORIENTED_EDGE('',*,*,#4526,.F.) ;
#6288=ORIENTED_EDGE('',*,*,#4519,.F.) ;
#6289=ORIENTED_EDGE('',*,*,#4538,.T.) ;
#6290=ORIENTED_EDGE('',*,*,#4523,.F.) ;
#6291=ORIENTED_EDGE('',*,*,#4530,.F.) ;
#6292=ORIENTED_EDGE('',*,*,#4539,.F.) ;
#6293=ORIENTED_EDGE('',*,*,#4509,.T.) ;
#6294=ORIENTED_EDGE('',*,*,#4532,.F.) ;
#6295=ORIENTED_EDGE('',*,*,#4527,.F.) ;
#6296=ORIENTED_EDGE('',*,*,#4537,.T.) ;
#6297=ORIENTED_EDGE('',*,*,#4540,.T.) ;
#6298=ORIENTED_EDGE('',*,*,#4541,.T.) ;
#6299=ORIENTED_EDGE('',*,*,#4542,.F.) ;
#6300=ORIENTED_EDGE('',*,*,#4539,.T.) ;
#6301=ORIENTED_EDGE('',*,*,#4529,.T.) ;
#6302=ORIENTED_EDGE('',*,*,#4534,.F.) ;
#6303=ORIENTED_EDGE('',*,*,#4543,.F.) ;
#6304=ORIENTED_EDGE('',*,*,#4544,.F.) ;
#6305=ORIENTED_EDGE('',*,*,#4545,.T.) ;
#6306=ORIENTED_EDGE('',*,*,#4546,.F.) ;
#6307=ORIENTED_EDGE('',*,*,#4547,.T.) ;
#6308=ORIENTED_EDGE('',*,*,#4548,.T.) ;
#6309=ORIENTED_EDGE('',*,*,#4549,.F.) ;
#6310=ORIENTED_EDGE('',*,*,#4541,.F.) ;
#6311=ORIENTED_EDGE('',*,*,#4550,.T.) ;
#6312=ORIENTED_EDGE('',*,*,#4546,.T.) ;
#6313=ORIENTED_EDGE('',*,*,#4551,.F.) ;
#6314=ORIENTED_EDGE('',*,*,#4536,.T.) ;
#6315=ORIENTED_EDGE('',*,*,#4547,.F.) ;
#6316=ORIENTED_EDGE('',*,*,#4550,.F.) ;
#6317=ORIENTED_EDGE('',*,*,#4540,.F.) ;
#6318=ORIENTED_EDGE('',*,*,#4542,.T.) ;
#6319=ORIENTED_EDGE('',*,*,#4551,.T.) ;
#6320=ORIENTED_EDGE('',*,*,#4549,.T.) ;
#6321=ORIENTED_EDGE('',*,*,#4538,.F.) ;
#6322=ORIENTED_EDGE('',*,*,#4552,.F.) ;
#6323=ORIENTED_EDGE('',*,*,#4553,.T.) ;
#6324=ORIENTED_EDGE('',*,*,#4554,.T.) ;
#6325=ORIENTED_EDGE('',*,*,#4555,.F.) ;
#6326=ORIENTED_EDGE('',*,*,#4533,.F.) ;
#6327=ORIENTED_EDGE('',*,*,#4545,.F.) ;
#6328=ORIENTED_EDGE('',*,*,#4556,.F.) ;
#6329=ORIENTED_EDGE('',*,*,#4553,.F.) ;
#6330=ORIENTED_EDGE('',*,*,#4554,.F.) ;
#6331=ORIENTED_EDGE('',*,*,#4556,.T.) ;
#6332=ORIENTED_EDGE('',*,*,#4544,.T.) ;
#6333=ORIENTED_EDGE('',*,*,#4557,.F.) ;
#6334=ORIENTED_EDGE('',*,*,#4555,.T.) ;
#6335=ORIENTED_EDGE('',*,*,#4557,.T.) ;
#6336=ORIENTED_EDGE('',*,*,#4543,.T.) ;
#6337=ORIENTED_EDGE('',*,*,#4535,.T.) ;
#6338=ORIENTED_EDGE('',*,*,#4548,.F.) ;
#6339=ORIENTED_EDGE('',*,*,#4518,.T.) ;
#6340=ORIENTED_EDGE('',*,*,#4552,.T.) ;
#6341=ORIENTED_EDGE('',*,*,#4524,.F.) ;
#6890=CONICAL_SURFACE('',#8198,1.5,0.785398163397) ;
#6891=CONICAL_SURFACE('',#8202,1.2,0.785398163397) ;
#7199=ADVANCED_FACE('',(#949),#640,.T.) ;
#7200=ADVANCED_FACE('',(#950),#6890,.T.) ;
#7201=ADVANCED_FACE('',(#951),#641,.T.) ;
#7202=ADVANCED_FACE('',(#952),#6891,.T.) ;
#7203=ADVANCED_FACE('',(#953),#416,.F.) ;
#7204=ADVANCED_FACE('',(#954),#417,.T.) ;
#7205=ADVANCED_FACE('',(#955),#418,.F.) ;
#7206=ADVANCED_FACE('',(#956),#419,.T.) ;
#7207=ADVANCED_FACE('',(#957),#420,.F.) ;
#7208=ADVANCED_FACE('',(#958),#421,.T.) ;
#7209=ADVANCED_FACE('',(#959),#422,.T.) ;
#7210=ADVANCED_FACE('',(#960),#423,.F.) ;
#7211=ADVANCED_FACE('',(#961),#424,.F.) ;
#7212=ADVANCED_FACE('',(#962,#244),#425,.T.) ;
#7213=ADVANCED_FACE('',(#963),#426,.F.) ;
#7214=ADVANCED_FACE('',(#964),#427,.F.) ;
#7215=ADVANCED_FACE('',(#965),#428,.F.) ;
#7216=ADVANCED_FACE('',(#966),#429,.T.) ;
#7217=ADVANCED_FACE('',(#967),#430,.T.) ;
#7218=ADVANCED_FACE('',(#968),#431,.F.) ;
#7219=ADVANCED_FACE('',(#969),#432,.T.) ;
#7220=ADVANCED_FACE('',(#970),#433,.T.) ;
#7221=ADVANCED_FACE('',(#971),#434,.T.) ;
#7379=CLOSED_SHELL('',(#7199,#7200,#7201,#7202,#7203,#7204,#7205,#7206,
#7207,#7208,#7209,#7210,#7211,#7212,#7213,#7214,#7215,#7216,#7217,#7218,
#7219,#7220,#7221)) ;
#8194=AXIS2_PLACEMENT_3D('',#12764,#10173,#10174) ;
#8195=AXIS2_PLACEMENT_3D('',#12765,#10175,#10176) ;
#8196=AXIS2_PLACEMENT_3D('',#12767,#10177,#10178) ;
#8197=AXIS2_PLACEMENT_3D('',#12770,#10180,#10181) ;
#8198=AXIS2_PLACEMENT_3D('',#12771,#10182,#10183) ;
#8199=AXIS2_PLACEMENT_3D('',#12774,#10185,#10186) ;
#8200=AXIS2_PLACEMENT_3D('',#12775,#10187,#10188) ;
#8201=AXIS2_PLACEMENT_3D('',#12778,#10190,#10191) ;
#8202=AXIS2_PLACEMENT_3D('',#12779,#10192,#10193) ;
#8203=AXIS2_PLACEMENT_3D('',#12782,#10195,#10196) ;
#8204=AXIS2_PLACEMENT_3D('',#12783,#10197,#10198) ;
#8205=AXIS2_PLACEMENT_3D('',#12784,#10199,#10200) ;
#8206=AXIS2_PLACEMENT_3D('',#12793,#10205,#10206) ;
#8207=AXIS2_PLACEMENT_3D('',#12802,#10211,#10212) ;
#8208=AXIS2_PLACEMENT_3D('',#12808,#10216,#10217) ;
#8209=AXIS2_PLACEMENT_3D('',#12814,#10221,#10222) ;
#8210=AXIS2_PLACEMENT_3D('',#12818,#10225,#10226) ;
#8211=AXIS2_PLACEMENT_3D('',#12822,#10229,#10230) ;
#8212=AXIS2_PLACEMENT_3D('',#12826,#10233,#10234) ;
#8213=AXIS2_PLACEMENT_3D('',#12830,#10237,#10238) ;
#8214=AXIS2_PLACEMENT_3D('',#12841,#10245,#10246) ;
#8215=AXIS2_PLACEMENT_3D('',#12848,#10251,#10252) ;
#8216=AXIS2_PLACEMENT_3D('',#12851,#10255,#10256) ;
#8217=AXIS2_PLACEMENT_3D('',#12852,#10257,#10258) ;
#8218=AXIS2_PLACEMENT_3D('',#12853,#10259,#10260) ;
#8219=AXIS2_PLACEMENT_3D('',#12860,#10265,#10266) ;
#8220=AXIS2_PLACEMENT_3D('',#12862,#10268,#10269) ;
#8221=AXIS2_PLACEMENT_3D('',#12864,#10271,#10272) ;
#8222=AXIS2_PLACEMENT_3D('',#12865,#10273,#10274) ;
#10173=DIRECTION('axis',(0.,0.,1.)) ;
#10174=DIRECTION('refdir',(1.,0.,0.)) ;
#10175=DIRECTION('center_axis',(0.,0.,1.)) ;
#10176=DIRECTION('ref_axis',(-0.999721561817394,0.0235965852909093,0.)) ;
#10177=DIRECTION('center_axis',(0.,0.,1.)) ;
#10178=DIRECTION('ref_axis',(-1.,0.,0.)) ;
#10179=DIRECTION('',(0.,0.,-1.)) ;
#10180=DIRECTION('center_axis',(0.,0.,1.)) ;
#10181=DIRECTION('ref_axis',(-1.,0.,0.)) ;
#10182=DIRECTION('center_axis',(0.,0.,1.)) ;
#10183=DIRECTION('ref_axis',(-0.999721561817394,0.0235965852909093,0.)) ;
#10184=DIRECTION('',(-0.706909895659168,0.0166853054720411,-0.707106781186864)) ;
#10185=DIRECTION('center_axis',(0.,0.,1.)) ;
#10186=DIRECTION('ref_axis',(-1.,0.,0.)) ;
#10187=DIRECTION('center_axis',(0.,0.,1.)) ;
#10188=DIRECTION('ref_axis',(-0.999721561817394,0.0235965852909093,0.)) ;
#10189=DIRECTION('',(0.,0.,-1.)) ;
#10190=DIRECTION('center_axis',(0.,0.,1.)) ;
#10191=DIRECTION('ref_axis',(-1.,0.,0.)) ;
#10192=DIRECTION('center_axis',(0.,0.,1.)) ;
#10193=DIRECTION('ref_axis',(-0.999721561817394,0.0235965852909093,0.)) ;
#10194=DIRECTION('',(-0.706909895659168,0.0166853054720411,-0.707106781186865)) ;
#10195=DIRECTION('center_axis',(0.,0.,1.)) ;
#10196=DIRECTION('ref_axis',(-1.,0.,0.)) ;
#10197=DIRECTION('center_axis',(0.,0.,1.)) ;
#10198=DIRECTION('ref_axis',(1.,0.,0.)) ;
#10199=DIRECTION('center_axis',(-0.612372435695786,0.353553390592877,0.707106781186753)) ;
#10200=DIRECTION('ref_axis',(0.612372435696143,-0.353553390593082,0.707106781186342)) ;
#10201=DIRECTION('',(0.50000000000019,0.866025403784329,0.)) ;
#10202=DIRECTION('',(0.612372435695786,-0.353553390592877,0.707106781186753)) ;
#10203=DIRECTION('',(0.50000000000019,0.866025403784329,0.)) ;
#10204=DIRECTION('',(0.612372435695786,-0.353553390592877,0.707106781186753)) ;
#10205=DIRECTION('center_axis',(-0.612372435695786,0.353553390592877,-0.707106781186753)) ;
#10206=DIRECTION('ref_axis',(-0.612372435696143,0.353553390593082,0.707106781186342)) ;
#10207=DIRECTION('',(0.50000000000019,0.866025403784329,0.)) ;
#10208=DIRECTION('',(-0.612372435695786,0.353553390592877,0.707106781186753)) ;
#10209=DIRECTION('',(0.50000000000019,0.866025403784329,0.)) ;
#10210=DIRECTION('',(-0.612372435695786,0.353553390592877,0.707106781186753)) ;
#10211=DIRECTION('center_axis',(-0.866025403784329,0.50000000000019,0.)) ;
#10212=DIRECTION('ref_axis',(0.,0.,1.)) ;
#10213=DIRECTION('',(0.,0.,1.)) ;
#10214=DIRECTION('',(0.50000000000019,0.866025403784329,0.)) ;
#10215=DIRECTION('',(0.,0.,1.)) ;
#10216=DIRECTION('center_axis',(-0.866025403784329,0.50000000000019,0.)) ;
#10217=DIRECTION('ref_axis',(0.,0.,1.)) ;
#10218=DIRECTION('',(0.50000000000019,0.866025403784329,0.)) ;
#10219=DIRECTION('',(0.,0.,1.)) ;
#10220=DIRECTION('',(0.,0.,1.)) ;
#10221=DIRECTION('center_axis',(-0.50000000000019,-0.866025403784329,0.)) ;
#10222=DIRECTION('ref_axis',(0.866025403784329,-0.50000000000019,0.)) ;
#10223=DIRECTION('',(-0.866025403784329,0.50000000000019,0.)) ;
#10224=DIRECTION('',(0.,0.,-1.)) ;
#10225=DIRECTION('center_axis',(-0.50000000000019,-0.866025403784329,0.)) ;
#10226=DIRECTION('ref_axis',(0.866025403784329,-0.50000000000019,0.)) ;
#10227=DIRECTION('',(0.866025403784329,-0.50000000000019,0.)) ;
#10228=DIRECTION('',(0.,0.,-1.)) ;
#10229=DIRECTION('center_axis',(-0.50000000000019,-0.866025403784329,0.)) ;
#10230=DIRECTION('ref_axis',(0.866025403784329,-0.50000000000019,0.)) ;
#10231=DIRECTION('',(0.,0.,-1.)) ;
#10232=DIRECTION('',(-0.866025403784329,0.50000000000019,0.)) ;
#10233=DIRECTION('center_axis',(-0.50000000000019,-0.866025403784329,0.)) ;
#10234=DIRECTION('ref_axis',(0.866025403784329,-0.50000000000019,0.)) ;
#10235=DIRECTION('',(0.,0.,-1.)) ;
#10236=DIRECTION('',(0.866025403784329,-0.50000000000019,0.)) ;
#10237=DIRECTION('center_axis',(0.,0.,1.)) ;
#10238=DIRECTION('ref_axis',(1.,0.,0.)) ;
#10239=DIRECTION('',(0.50000000000019,0.866025403784329,0.)) ;
#10240=DIRECTION('',(-0.866025403784329,0.50000000000019,0.)) ;
#10241=DIRECTION('',(0.50000000000019,0.866025403784329,0.)) ;
#10242=DIRECTION('',(-0.50000000000019,-0.866025403784329,0.)) ;
#10243=DIRECTION('',(-0.866025403784329,0.50000000000019,0.)) ;
#10244=DIRECTION('',(-0.50000000000019,-0.866025403784329,0.)) ;
#10245=DIRECTION('center_axis',(-0.353553390592877,-0.612372435695786,-0.707106781186753)) ;
#10246=DIRECTION('ref_axis',(-0.353553390593082,-0.612372435696143,0.707106781186342)) ;
#10247=DIRECTION('',(-0.866025403784329,0.50000000000019,0.)) ;
#10248=DIRECTION('',(-0.353553390592877,-0.612372435695786,0.707106781186753)) ;
#10249=DIRECTION('',(-0.866025403784329,0.50000000000019,0.)) ;
#10250=DIRECTION('',(-0.353553390592877,-0.612372435695786,0.707106781186753)) ;
#10251=DIRECTION('center_axis',(-0.50000000000019,-0.866025403784329,0.)) ;
#10252=DIRECTION('ref_axis',(0.,0.,1.)) ;
#10253=DIRECTION('',(0.,0.,1.)) ;
#10254=DIRECTION('',(0.,0.,1.)) ;
#10255=DIRECTION('center_axis',(0.866025403784329,-0.50000000000019,0.)) ;
#10256=DIRECTION('ref_axis',(0.50000000000019,0.866025403784329,0.)) ;
#10257=DIRECTION('center_axis',(0.866025403784329,-0.50000000000019,0.)) ;
#10258=DIRECTION('ref_axis',(0.50000000000019,0.866025403784329,0.)) ;
#10259=DIRECTION('center_axis',(-0.353553390592877,-0.612372435695786,0.707106781186753)) ;
#10260=DIRECTION('ref_axis',(0.353553390593082,0.612372435696143,0.707106781186342)) ;
#10261=DIRECTION('',(-0.866025403784329,0.50000000000019,0.)) ;
#10262=DIRECTION('',(0.353553390592877,0.612372435695786,0.707106781186753)) ;
#10263=DIRECTION('',(-0.866025403784329,0.50000000000019,0.)) ;
#10264=DIRECTION('',(0.353553390592877,0.612372435695786,0.707106781186753)) ;
#10265=DIRECTION('center_axis',(0.866025403784329,-0.50000000000019,0.)) ;
#10266=DIRECTION('ref_axis',(0.50000000000019,0.866025403784329,0.)) ;
#10267=DIRECTION('',(0.,0.,1.)) ;
#10268=DIRECTION('center_axis',(-0.50000000000019,-0.866025403784329,0.)) ;
#10269=DIRECTION('ref_axis',(0.,0.,1.)) ;
#10270=DIRECTION('',(0.,0.,1.)) ;
#10271=DIRECTION('center_axis',(0.866025403784329,-0.50000000000019,0.)) ;
#10272=DIRECTION('ref_axis',(0.50000000000019,0.866025403784329,0.)) ;
#10273=DIRECTION('center_axis',(0.,0.,1.)) ;
#10274=DIRECTION('ref_axis',(0.,1.,0.)) ;
#12764=CARTESIAN_POINT('',(0.,0.,0.)) ;
#12765=CARTESIAN_POINT('Origin',(-21.6506350946,12.5,128.75)) ;
#12766=CARTESIAN_POINT('',(-19.0513590339,12.4386488782,143.75)) ;
#12767=CARTESIAN_POINT('Origin',(-21.6506350946,12.5,143.75)) ;
#12768=CARTESIAN_POINT('',(-19.0513590339,12.4386488782,143.25)) ;
#12769=CARTESIAN_POINT('',(-19.0513590338748,12.4386488782436,128.75)) ;
#12770=CARTESIAN_POINT('Origin',(-21.6506350946,12.5,143.25)) ;
#12771=CARTESIAN_POINT('Origin',(-21.6506350946,12.5,142.15)) ;
#12772=CARTESIAN_POINT('',(-20.1510527519,12.4646051221,142.15)) ;
#12773=CARTESIAN_POINT('',(-20.1510527518739,12.4646051220636,142.15)) ;
#12774=CARTESIAN_POINT('Origin',(-21.6506350946,12.5,142.15)) ;
#12775=CARTESIAN_POINT('Origin',(-21.6506350946,12.5,128.75)) ;
#12776=CARTESIAN_POINT('',(-20.1510527519,12.4646051221,114.05)) ;
#12777=CARTESIAN_POINT('',(-20.1510527518739,12.4646051220636,128.75)) ;
#12778=CARTESIAN_POINT('Origin',(-21.6506350946,12.5,114.05)) ;
#12779=CARTESIAN_POINT('Origin',(-21.6506350946,12.5,113.75)) ;
#12780=CARTESIAN_POINT('',(-20.4509692204,12.4716840977,113.75)) ;
#12781=CARTESIAN_POINT('',(-20.4509692204191,12.4716840976509,113.75)) ;
#12782=CARTESIAN_POINT('Origin',(-21.6506350946,12.5,113.75)) ;
#12783=CARTESIAN_POINT('Origin',(0.,-26.2,113.75)) ;
#12784=CARTESIAN_POINT('Origin',(-21.3042249331,12.3,142.25)) ;
#12785=CARTESIAN_POINT('',(-21.5042249331,11.9535898385,142.25)) ;
#12786=CARTESIAN_POINT('',(-21.1042249331,12.6464101615,142.25)) ;
#12787=CARTESIAN_POINT('',(-21.2042249331,12.4732050808,142.25)) ;
#12788=CARTESIAN_POINT('',(-20.335090638,11.2785898385,143.6)) ;
#12789=CARTESIAN_POINT('',(-20.9196577855,11.6160898385,142.925)) ;
#12790=CARTESIAN_POINT('',(-19.935090638,11.9714101615,143.6)) ;
#12791=CARTESIAN_POINT('',(-20.135090638,11.625,143.6)) ;
#12792=CARTESIAN_POINT('',(-20.5196577855,12.3089101615,142.925)) ;
#12793=CARTESIAN_POINT('Origin',(-21.9970452561,12.7,142.25)) ;
#12794=CARTESIAN_POINT('',(-23.3661795512,13.0285898385,143.6)) ;
#12795=CARTESIAN_POINT('',(-22.9661795512,13.7214101615,143.6)) ;
#12796=CARTESIAN_POINT('',(-23.1661795512,13.375,143.6)) ;
#12797=CARTESIAN_POINT('',(-22.1970452561,12.3535898385,142.25)) ;
#12798=CARTESIAN_POINT('',(-22.7816124037,12.6910898385,142.925)) ;
#12799=CARTESIAN_POINT('',(-21.7970452561,13.0464101615,142.25)) ;
#12800=CARTESIAN_POINT('',(-22.0970452561,12.5267949192,142.25)) ;
#12801=CARTESIAN_POINT('',(-22.3816124037,13.3839101615,142.925)) ;
#12802=CARTESIAN_POINT('Origin',(-20.135090638,11.625,143.6)) ;
#12803=CARTESIAN_POINT('',(-20.335090638,11.2785898385,143.75)) ;
#12804=CARTESIAN_POINT('',(-20.335090638,11.2785898385,143.675)) ;
#12805=CARTESIAN_POINT('',(-19.935090638,11.9714101615,143.75)) ;
#12806=CARTESIAN_POINT('',(-20.135090638,11.625,143.75)) ;
#12807=CARTESIAN_POINT('',(-19.935090638,11.9714101615,143.675)) ;
#12808=CARTESIAN_POINT('Origin',(-23.1661795512,13.375,143.6)) ;
#12809=CARTESIAN_POINT('',(-23.3661795512,13.0285898385,143.75)) ;
#12810=CARTESIAN_POINT('',(-22.9661795512,13.7214101615,143.75)) ;
#12811=CARTESIAN_POINT('',(-23.1661795512,13.375,143.75)) ;
#12812=CARTESIAN_POINT('',(-23.3661795512,13.0285898385,143.675)) ;
#12813=CARTESIAN_POINT('',(-22.9661795512,13.7214101615,143.675)) ;
#12814=CARTESIAN_POINT('Origin',(0.2,0.346410161514,0.)) ;
#12815=CARTESIAN_POINT('',(-21.1042249331,12.6464101615,143.75)) ;
#12816=CARTESIAN_POINT('',(-20.5196577855,12.3089101615,143.75)) ;
#12817=CARTESIAN_POINT('',(-21.1042249331,12.6464101615,143.)) ;
#12818=CARTESIAN_POINT('Origin',(0.2,0.346410161514,0.)) ;
#12819=CARTESIAN_POINT('',(-21.7970452561,13.0464101615,143.75)) ;
#12820=CARTESIAN_POINT('',(-22.3816124037,13.3839101615,143.75)) ;
#12821=CARTESIAN_POINT('',(-21.7970452561,13.0464101615,143.)) ;
#12822=CARTESIAN_POINT('Origin',(-0.2,-0.346410161514,0.)) ;
#12823=CARTESIAN_POINT('',(-21.5042249331,11.9535898385,143.75)) ;
#12824=CARTESIAN_POINT('',(-21.5042249331,11.9535898385,143.)) ;
#12825=CARTESIAN_POINT('',(-20.9196577855,11.6160898385,143.75)) ;
#12826=CARTESIAN_POINT('Origin',(-0.2,-0.346410161514,0.)) ;
#12827=CARTESIAN_POINT('',(-22.1970452561,12.3535898385,143.75)) ;
#12828=CARTESIAN_POINT('',(-22.1970452561,12.3535898385,143.)) ;
#12829=CARTESIAN_POINT('',(-22.7816124037,12.6910898385,143.75)) ;
#12830=CARTESIAN_POINT('Origin',(0.,-25.,143.75)) ;
#12831=CARTESIAN_POINT('',(-22.1792249331,10.7844555434,143.75)) ;
#12832=CARTESIAN_POINT('',(-21.8417249331,11.3690226909,143.75)) ;
#12833=CARTESIAN_POINT('',(-22.8720452561,11.1844555434,143.75)) ;
#12834=CARTESIAN_POINT('',(-22.5256350946,10.9844555434,143.75)) ;
#12835=CARTESIAN_POINT('',(-22.5345452561,11.7690226909,143.75)) ;
#12836=CARTESIAN_POINT('',(-21.1220452561,14.2155444566,143.75)) ;
#12837=CARTESIAN_POINT('',(-21.4595452561,13.6309773091,143.75)) ;
#12838=CARTESIAN_POINT('',(-20.4292249331,13.8155444566,143.75)) ;
#12839=CARTESIAN_POINT('',(-20.7756350946,14.0155444566,143.75)) ;
#12840=CARTESIAN_POINT('',(-20.7667249331,13.2309773091,143.75)) ;
#12841=CARTESIAN_POINT('Origin',(-21.8506350946,12.1535898385,142.25)) ;
#12842=CARTESIAN_POINT('',(-22.1792249331,10.7844555434,143.6)) ;
#12843=CARTESIAN_POINT('',(-22.8720452561,11.1844555434,143.6)) ;
#12844=CARTESIAN_POINT('',(-22.5256350946,10.9844555434,143.6)) ;
#12845=CARTESIAN_POINT('',(-21.8417249331,11.3690226909,142.925)) ;
#12846=CARTESIAN_POINT('',(-21.6774300139,12.0535898385,142.25)) ;
#12847=CARTESIAN_POINT('',(-22.5345452561,11.7690226909,142.925)) ;
#12848=CARTESIAN_POINT('Origin',(-22.5256350946,10.9844555434,143.6)) ;
#12849=CARTESIAN_POINT('',(-22.1792249331,10.7844555434,143.675)) ;
#12850=CARTESIAN_POINT('',(-22.8720452561,11.1844555434,143.675)) ;
#12851=CARTESIAN_POINT('Origin',(-8.8042249331,33.9506350946,0.)) ;
#12852=CARTESIAN_POINT('Origin',(-9.49704525612,34.3506350946,0.)) ;
#12853=CARTESIAN_POINT('Origin',(-21.4506350946,12.8464101615,142.25)) ;
#12854=CARTESIAN_POINT('',(-21.6238401754,12.9464101615,142.25)) ;
#12855=CARTESIAN_POINT('',(-20.4292249331,13.8155444566,143.6)) ;
#12856=CARTESIAN_POINT('',(-20.7667249331,13.2309773091,142.925)) ;
#12857=CARTESIAN_POINT('',(-21.1220452561,14.2155444566,143.6)) ;
#12858=CARTESIAN_POINT('',(-20.7756350946,14.0155444566,143.6)) ;
#12859=CARTESIAN_POINT('',(-21.4595452561,13.6309773091,142.925)) ;
#12860=CARTESIAN_POINT('Origin',(-8.8042249331,33.9506350946,0.)) ;
#12861=CARTESIAN_POINT('',(-20.4292249331,13.8155444566,143.675)) ;
#12862=CARTESIAN_POINT('Origin',(-20.7756350946,14.0155444566,143.6)) ;
#12863=CARTESIAN_POINT('',(-21.1220452561,14.2155444566,143.675)) ;
#12864=CARTESIAN_POINT('Origin',(-9.49704525612,34.3506350946,0.)) ;
#12865=CARTESIAN_POINT('Origin',(0.,-25.,142.25)) ;
#13485=UNCERTAINTY_MEASURE_WITH_UNIT(LENGTH_MEASURE(0.01),#13511,
'DISTANCE_ACCURACY_VALUE',
'Maximum model space distance between geometric entities at asserted c
onnectivities') ;
#13493=UNCERTAINTY_MEASURE_WITH_UNIT(LENGTH_MEASURE(0.01),#13511,
'DISTANCE_ACCURACY_VALUE',
'Maximum model space distance between geometric entities at asserted c
onnectivities') ;
#13502=(
GEOMETRIC_REPRESENTATION_CONTEXT(3)
GLOBAL_UNCERTAINTY_ASSIGNED_CONTEXT((#13485))
GLOBAL_UNIT_ASSIGNED_CONTEXT((#13511,#13513,#13514))
REPRESENTATION_CONTEXT('','3D')
) ;
#13510=(
GEOMETRIC_REPRESENTATION_CONTEXT(3)
GLOBAL_UNCERTAINTY_ASSIGNED_CONTEXT((#13493))
GLOBAL_UNIT_ASSIGNED_CONTEXT((#13511,#13513,#13514))
REPRESENTATION_CONTEXT('','3D')
) ;
#13511=(
LENGTH_UNIT()
NAMED_UNIT(*)
SI_UNIT(.MILLI.,.METRE.)
) ;
#13513=(
NAMED_UNIT(*)
PLANE_ANGLE_UNIT()
SI_UNIT($,.RADIAN.)
) ;
#13514=(
NAMED_UNIT(*)
SI_UNIT($,.STERADIAN.)
SOLID_ANGLE_UNIT()
) ;
#13523=SHAPE_DEFINITION_REPRESENTATION(#13539,#13570) ;
#13539=PRODUCT_DEFINITION_SHAPE('',$,#13587) ;
#13570=SHAPE_REPRESENTATION('',(#8194),#13502) ;
#13578=PRODUCT_DEFINITION_CONTEXT('part definition',#13628,'design') ;
#13587=PRODUCT_DEFINITION('Cover_Screw_2','Cover_Screw_2',#13603,#13578) ;
#13603=PRODUCT_DEFINITION_FORMATION('',$,#13638) ;
#13628=APPLICATION_CONTEXT(
'Core Data for Automotive Mechanical Design Process') ;
#13629=PRODUCT_CONTEXT('part definition',#13628,'mechanical') ;
#13638=PRODUCT('Cover_Screw_2','Cover_Screw_2',$,(#13629)) ;
#13650=PRESENTATION_STYLE_ASSIGNMENT((#13655)) ;
#13655=SURFACE_STYLE_USAGE(.BOTH.,#13660) ;
#13660=SURFACE_SIDE_STYLE('',(#13665)) ;
#13665=SURFACE_STYLE_FILL_AREA(#13670) ;
#13670=FILL_AREA_STYLE('Opaque(144,144,144)',(#13675)) ;
#13675=FILL_AREA_STYLE_COLOUR('Opaque(144,144,144)',#13680) ;
#13680=COLOUR_RGB('Opaque(144,144,144)', 0.40784314, 0.44705882, 0.49803922) ;
ENDSEC;
END-ISO-10303-21;
